ISO-10303-21;
HEADER;
/* Generated by software containing ST-Developer
 * from STEP Tools, Inc. (www.steptools.com) 
 */

FILE_DESCRIPTION(
/* description */ ('Torque wrench calibration arm'),
/* implementation_level */ '2;1');

FILE_NAME(
/* name */ 'Seals 2RS (1).step',
/* time_stamp */ '2026-10-28T03:24:52-07:00',
/* author */ (''),
/* organization */ (''),
/* preprocessor_version */ 'ST-DEVELOPER v20.2',
/* originating_system */ 'Autodesk Translation Framework v15.17.0.0',
/* authorisation */ '');

FILE_SCHEMA (('AUTOMOTIVE_DESIGN { 1 0 10303 214 3 1 1 }'));
ENDSEC;

DATA;
#10=MECHANICAL_DESIGN_GEOMETRIC_PRESENTATION_REPRESENTATION('',(#469,#470),#12783);
#379=SHAPE_REPRESENTATION_RELATIONSHIP('SRR','None',#12963,#416);
#416=ADVANCED_BREP_SHAPE_REPRESENTATION('',(#521,#522),#12772);
#469=STYLED_ITEM('',(#13212),#521);
#470=STYLED_ITEM('',(#13212),#522);
#521=MANIFOLD_SOLID_BREP('Body1',#6540);
#522=MANIFOLD_SOLID_BREP('Body2',#6541);
#627=FACE_BOUND('',#1694,.T.);
#628=FACE_BOUND('',#1697,.T.);
#629=FACE_BOUND('',#1700,.T.);
#630=FACE_BOUND('',#1703,.T.);
#834=PLANE('',#7650);
#835=PLANE('',#7655);
#836=PLANE('',#7658);
#837=PLANE('',#7663);
#1202=FACE_OUTER_BOUND('',#1693,.T.);
#1203=FACE_OUTER_BOUND('',#1695,.T.);
#1204=FACE_OUTER_BOUND('',#1696,.T.);
#1205=FACE_OUTER_BOUND('',#1698,.T.);
#1206=FACE_OUTER_BOUND('',#1699,.T.);
#1207=FACE_OUTER_BOUND('',#1701,.T.);
#1208=FACE_OUTER_BOUND('',#1702,.T.);
#1209=FACE_OUTER_BOUND('',#1704,.T.);
#1693=EDGE_LOOP('',(#5747));
#1694=EDGE_LOOP('',(#5748));
#1695=EDGE_LOOP('',(#5749,#5750,#5751,#5752));
#1696=EDGE_LOOP('',(#5753));
#1697=EDGE_LOOP('',(#5754));
#1698=EDGE_LOOP('',(#5755,#5756,#5757,#5758));
#1699=EDGE_LOOP('',(#5759));
#1700=EDGE_LOOP('',(#5760));
#1701=EDGE_LOOP('',(#5761,#5762,#5763,#5764));
#1702=EDGE_LOOP('',(#5765));
#1703=EDGE_LOOP('',(#5766));
#1704=EDGE_LOOP('',(#5767,#5768,#5769,#5770));
#2132=LINE('',#12396,#2547);
#2133=LINE('',#12401,#2548);
#2134=LINE('',#12410,#2549);
#2135=LINE('',#12415,#2550);
#2547=VECTOR('',#9546,1.013815);
#2548=VECTOR('',#9553,0.991185);
#2549=VECTOR('',#9564,1.013815);
#2550=VECTOR('',#9571,0.991185);
#2920=CIRCLE('',#7651,1.013815);
#2921=CIRCLE('',#7652,0.991185);
#2922=CIRCLE('',#7654,1.013815);
#2923=CIRCLE('',#7656,0.991185);
#2924=CIRCLE('',#7659,1.013815);
#2925=CIRCLE('',#7660,0.991185);
#2926=CIRCLE('',#7662,1.013815);
#2927=CIRCLE('',#7664,0.991185);
#3454=VERTEX_POINT('',#12389);
#3455=VERTEX_POINT('',#12391);
#3456=VERTEX_POINT('',#12394);
#3457=VERTEX_POINT('',#12398);
#3458=VERTEX_POINT('',#12403);
#3459=VERTEX_POINT('',#12405);
#3460=VERTEX_POINT('',#12408);
#3461=VERTEX_POINT('',#12412);
#4231=EDGE_CURVE('',#3454,#3454,#2920,.T.);
#4232=EDGE_CURVE('',#3455,#3455,#2921,.T.);
#4233=EDGE_CURVE('',#3456,#3456,#2922,.T.);
#4234=EDGE_CURVE('',#3456,#3454,#2132,.T.);
#4235=EDGE_CURVE('',#3457,#3457,#2923,.T.);
#4236=EDGE_CURVE('',#3457,#3455,#2133,.T.);
#4237=EDGE_CURVE('',#3458,#3458,#2924,.T.);
#4238=EDGE_CURVE('',#3459,#3459,#2925,.T.);
#4239=EDGE_CURVE('',#3460,#3460,#2926,.T.);
#4240=EDGE_CURVE('',#3460,#3458,#2134,.T.);
#4241=EDGE_CURVE('',#3461,#3461,#2927,.T.);
#4242=EDGE_CURVE('',#3461,#3459,#2135,.T.);
#5747=ORIENTED_EDGE('',*,*,#4231,.F.);
#5748=ORIENTED_EDGE('',*,*,#4232,.T.);
#5749=ORIENTED_EDGE('',*,*,#4233,.F.);
#5750=ORIENTED_EDGE('',*,*,#4234,.T.);
#5751=ORIENTED_EDGE('',*,*,#4231,.T.);
#5752=ORIENTED_EDGE('',*,*,#4234,.F.);
#5753=ORIENTED_EDGE('',*,*,#4233,.T.);
#5754=ORIENTED_EDGE('',*,*,#4235,.F.);
#5755=ORIENTED_EDGE('',*,*,#4235,.T.);
#5756=ORIENTED_EDGE('',*,*,#4236,.T.);
#5757=ORIENTED_EDGE('',*,*,#4232,.F.);
#5758=ORIENTED_EDGE('',*,*,#4236,.F.);
#5759=ORIENTED_EDGE('',*,*,#4237,.F.);
#5760=ORIENTED_EDGE('',*,*,#4238,.T.);
#5761=ORIENTED_EDGE('',*,*,#4239,.F.);
#5762=ORIENTED_EDGE('',*,*,#4240,.T.);
#5763=ORIENTED_EDGE('',*,*,#4237,.T.);
#5764=ORIENTED_EDGE('',*,*,#4240,.F.);
#5765=ORIENTED_EDGE('',*,*,#4239,.T.);
#5766=ORIENTED_EDGE('',*,*,#4241,.F.);
#5767=ORIENTED_EDGE('',*,*,#4241,.T.);
#5768=ORIENTED_EDGE('',*,*,#4242,.T.);
#5769=ORIENTED_EDGE('',*,*,#4238,.F.);
#5770=ORIENTED_EDGE('',*,*,#4242,.F.);
#6076=CYLINDRICAL_SURFACE('',#7653,1.013815);
#6077=CYLINDRICAL_SURFACE('',#7657,0.991185);
#6078=CYLINDRICAL_SURFACE('',#7661,1.013815);
#6079=CYLINDRICAL_SURFACE('',#7665,0.991185);
#6427=ADVANCED_FACE('',(#1202,#627),#834,.T.);
#6428=ADVANCED_FACE('',(#1203),#6076,.T.);
#6429=ADVANCED_FACE('',(#1204,#628),#835,.T.);
#6430=ADVANCED_FACE('',(#1205),#6077,.F.);
#6431=ADVANCED_FACE('',(#1206,#629),#836,.T.);
#6432=ADVANCED_FACE('',(#1207),#6078,.T.);
#6433=ADVANCED_FACE('',(#1208,#630),#837,.T.);
#6434=ADVANCED_FACE('',(#1209),#6079,.F.);
#6540=CLOSED_SHELL('',(#6427,#6428,#6429,#6430));
#6541=CLOSED_SHELL('',(#6431,#6432,#6433,#6434));
#7649=AXIS2_PLACEMENT_3D('',#12387,#9534,#9535);
#7650=AXIS2_PLACEMENT_3D('',#12388,#9536,#9537);
#7651=AXIS2_PLACEMENT_3D('',#12390,#9538,#9539);
#7652=AXIS2_PLACEMENT_3D('',#12392,#9540,#9541);
#7653=AXIS2_PLACEMENT_3D('',#12393,#9542,#9543);
#7654=AXIS2_PLACEMENT_3D('',#12395,#9544,#9545);
#7655=AXIS2_PLACEMENT_3D('',#12397,#9547,#9548);
#7656=AXIS2_PLACEMENT_3D('',#12399,#9549,#9550);
#7657=AXIS2_PLACEMENT_3D('',#12400,#9551,#9552);
#7658=AXIS2_PLACEMENT_3D('',#12402,#9554,#9555);
#7659=AXIS2_PLACEMENT_3D('',#12404,#9556,#9557);
#7660=AXIS2_PLACEMENT_3D('',#12406,#9558,#9559);
#7661=AXIS2_PLACEMENT_3D('',#12407,#9560,#9561);
#7662=AXIS2_PLACEMENT_3D('',#12409,#9562,#9563);
#7663=AXIS2_PLACEMENT_3D('',#12411,#9565,#9566);
#7664=AXIS2_PLACEMENT_3D('',#12413,#9567,#9568);
#7665=AXIS2_PLACEMENT_3D('',#12414,#9569,#9570);
#9534=DIRECTION('axis',(0.,0.,1.));
#9535=DIRECTION('refdir',(1.,0.,0.));
#9536=DIRECTION('center_axis',(0.,1.,0.));
#9537=DIRECTION('ref_axis',(0.,0.,1.));
#9538=DIRECTION('center_axis',(0.,-1.,0.));
#9539=DIRECTION('ref_axis',(1.,0.,0.));
#9540=DIRECTION('center_axis',(0.,-1.,0.));
#9541=DIRECTION('ref_axis',(1.,0.,0.));
#9542=DIRECTION('center_axis',(0.,-1.,0.));
#9543=DIRECTION('ref_axis',(1.,0.,0.));
#9544=DIRECTION('center_axis',(0.,-1.,0.));
#9545=DIRECTION('ref_axis',(1.,0.,0.));
#9546=DIRECTION('',(0.,1.,0.));
#9547=DIRECTION('center_axis',(0.,-1.,0.));
#9548=DIRECTION('ref_axis',(0.,0.,-1.));
#9549=DIRECTION('center_axis',(0.,-1.,0.));
#9550=DIRECTION('ref_axis',(1.,0.,0.));
#9551=DIRECTION('center_axis',(0.,-1.,0.));
#9552=DIRECTION('ref_axis',(1.,0.,0.));
#9553=DIRECTION('',(0.,1.,0.));
#9554=DIRECTION('center_axis',(0.,1.,0.));
#9555=DIRECTION('ref_axis',(0.,0.,1.));
#9556=DIRECTION('center_axis',(0.,-1.,0.));
#9557=DIRECTION('ref_axis',(1.,0.,0.));
#9558=DIRECTION('center_axis',(0.,-1.,0.));
#9559=DIRECTION('ref_axis',(1.,0.,0.));
#9560=DIRECTION('center_axis',(0.,-1.,0.));
#9561=DIRECTION('ref_axis',(1.,0.,0.));
#9562=DIRECTION('center_axis',(0.,-1.,0.));
#9563=DIRECTION('ref_axis',(1.,0.,0.));
#9564=DIRECTION('',(0.,1.,0.));
#9565=DIRECTION('center_axis',(0.,-1.,0.));
#9566=DIRECTION('ref_axis',(0.,0.,-1.));
#9567=DIRECTION('center_axis',(0.,-1.,0.));
#9568=DIRECTION('ref_axis',(1.,0.,0.));
#9569=DIRECTION('center_axis',(0.,-1.,0.));
#9570=DIRECTION('ref_axis',(1.,0.,0.));
#9571=DIRECTION('',(0.,1.,0.));
#12387=CARTESIAN_POINT('',(0.,0.,0.));
#12388=CARTESIAN_POINT('Origin',(1.013815,0.445,0.));
#12389=CARTESIAN_POINT('',(-1.013815,0.445,-1.24156529467757E-16));
#12390=CARTESIAN_POINT('Origin',(0.,0.445,0.));
#12391=CARTESIAN_POINT('',(-0.991185,0.445,-1.21385153761287E-16));
#12392=CARTESIAN_POINT('Origin',(0.,0.445,0.));
#12393=CARTESIAN_POINT('Origin',(0.,0.4075,0.));
#12394=CARTESIAN_POINT('',(-1.013815,0.37,-1.24156529467757E-16));
#12395=CARTESIAN_POINT('Origin',(0.,0.37,0.));
#12396=CARTESIAN_POINT('',(-1.013815,0.4075,-1.24156529467757E-16));
#12397=CARTESIAN_POINT('Origin',(0.991185,0.37,0.));
#12398=CARTESIAN_POINT('',(-0.991185,0.37,-1.21385153761287E-16));
#12399=CARTESIAN_POINT('Origin',(0.,0.37,0.));
#12400=CARTESIAN_POINT('Origin',(0.,0.4075,0.));
#12401=CARTESIAN_POINT('',(-0.991185,0.4075,-1.21385153761287E-16));
#12402=CARTESIAN_POINT('Origin',(1.013815,-0.37,0.));
#12403=CARTESIAN_POINT('',(-1.013815,-0.37,-1.24156529467757E-16));
#12404=CARTESIAN_POINT('Origin',(0.,-0.37,0.));
#12405=CARTESIAN_POINT('',(-0.991185,-0.37,-1.21385153761287E-16));
#12406=CARTESIAN_POINT('Origin',(0.,-0.37,0.));
#12407=CARTESIAN_POINT('Origin',(0.,-0.4075,0.));
#12408=CARTESIAN_POINT('',(-1.013815,-0.445,-1.24156529467757E-16));
#12409=CARTESIAN_POINT('Origin',(0.,-0.445,0.));
#12410=CARTESIAN_POINT('',(-1.013815,-0.4075,-1.24156529467757E-16));
#12411=CARTESIAN_POINT('Origin',(0.991185,-0.445,0.));
#12412=CARTESIAN_POINT('',(-0.991185,-0.445,-1.21385153761287E-16));
#12413=CARTESIAN_POINT('Origin',(0.,-0.445,0.));
#12414=CARTESIAN_POINT('Origin',(0.,-0.4075,0.));
#12415=CARTESIAN_POINT('',(-0.991185,-0.4075,-1.21385153761287E-16));
#12728=UNCERTAINTY_MEASURE_WITH_UNIT(LENGTH_MEASURE(0.001),#12784,
'DISTANCE_ACCURACY_VALUE',
'Maximum model space distance between geometric entities at asserted c
onnectivities');
#12739=UNCERTAINTY_MEASURE_WITH_UNIT(LENGTH_MEASURE(0.001),#12784,
'DISTANCE_ACCURACY_VALUE',
'Maximum model space distance between geometric entities at asserted c
onnectivities');
#12772=(
GEOMETRIC_REPRESENTATION_CONTEXT(3)
GLOBAL_UNCERTAINTY_ASSIGNED_CONTEXT((#12728))
GLOBAL_UNIT_ASSIGNED_CONTEXT((#12784,#12786,#12787))
REPRESENTATION_CONTEXT('','3D')
);
#12783=(
GEOMETRIC_REPRESENTATION_CONTEXT(3)
GLOBAL_UNCERTAINTY_ASSIGNED_CONTEXT((#12739))
GLOBAL_UNIT_ASSIGNED_CONTEXT((#12784,#12786,#12787))
REPRESENTATION_CONTEXT('','3D')
);
#12784=(
LENGTH_UNIT()
NAMED_UNIT(*)
SI_UNIT(.CENTI.,.METRE.)
);
#12786=(
NAMED_UNIT(*)
PLANE_ANGLE_UNIT()
SI_UNIT($,.RADIAN.)
);
#12787=(
NAMED_UNIT(*)
SI_UNIT($,.STERADIAN.)
SOLID_ANGLE_UNIT()
);
#12820=SHAPE_DEFINITION_REPRESENTATION(#12889,#12963);
#12889=PRODUCT_DEFINITION_SHAPE('',$,#13007);
#12963=SHAPE_REPRESENTATION('',(#7649),#12772);
#12974=PRODUCT_DEFINITION_CONTEXT('part definition',#13105,'design');
#13007=PRODUCT_DEFINITION('Seals 2RS (1)','Seals 2RS (1)',#13050,#12974);
#13050=PRODUCT_DEFINITION_FORMATION('',$,#13139);
#13105=APPLICATION_CONTEXT(
'Core Data for Automotive Mechanical Design Process');
#13106=PRODUCT_CONTEXT('part definition',#13105,'mechanical');
#13139=PRODUCT('Seals 2RS (1)','Seals 2RS (1)','Seals 2RS (1)',(#13106));
#13206=COLOUR_RGB('Grey',0.48,0.52,0.57);
#13207=FILL_AREA_STYLE_COLOUR('',#13206);
#13208=FILL_AREA_STYLE('',(#13207));
#13209=SURFACE_STYLE_FILL_AREA(#13208);
#13210=SURFACE_SIDE_STYLE('',(#13209));
#13211=SURFACE_STYLE_USAGE(.BOTH.,#13210);
#13212=PRESENTATION_STYLE_ASSIGNMENT((#13211));
ENDSEC;
END-ISO-10303-21;
